ISO-10303-21;
HEADER;
FILE_DESCRIPTION (('STEP AP214'),
    '1' );
FILE_NAME ('15. Washer M6.step',
    '2026-10-09T08:13:37',
    ( '' ),
    ( '' ),
    'SwSTEP 2.0',
    'SolidWorks 2021',
    '' );
FILE_SCHEMA (( 'AUTOMOTIVE_DESIGN' ));
ENDSEC;

DATA;
#9=ORIENTED_EDGE ( 'NONE', *, *, #4228, .F. ) ;
#754=DIRECTION ( 'NONE',  ( 0.000000000000000000, 0.000000000000000000, 1.000000000000000000 ) ) ;
#1026=CARTESIAN_POINT ( 'NONE',  ( 0.000000000000000000, 2.299999999999999822, 0.000000000000000000 ) ) ;
#1242=AXIS2_PLACEMENT_3D ( 'NONE', #13763, #56679, #8505 ) ;
#1866=LINE ( 'NONE', #23724, #57215 ) ;
#2089=VERTEX_POINT ( 'NONE', #12173 ) ;
#2381=AXIS2_PLACEMENT_3D ( 'NONE', #66229, #28220, #754 ) ;
#2397=CARTESIAN_POINT ( 'NONE',  ( 0.000000000000000000, 2.299999999999999822, 0.000000000000000000 ) ) ;
#3227=CYLINDRICAL_SURFACE ( 'NONE', #24188, 10.00000000000000000 ) ;
#3994=ORIENTED_EDGE ( 'NONE', *, *, #49735, .F. ) ;
#4138=CARTESIAN_POINT ( 'NONE',  ( 3.673940397442060361E-16, 0.000000000000000000, 3.000000000000000444 ) ) ;
#4228=EDGE_CURVE ( 'NONE', #44728, #11138, #62742, .T. ) ;
#4351=EDGE_CURVE ( 'NONE', #11138, #46046, #65655, .T. ) ;
#5099=CARTESIAN_POINT ( 'NONE',  ( 0.000000000000000000, 0.000000000000000000, -3.000000000000000444 ) ) ;
#5387=DIRECTION ( 'NONE',  ( 0.000000000000000000, -0.000000000000000000, 1.000000000000000000 ) ) ;
#5551=ORIENTED_EDGE ( 'NONE', *, *, #4228, .T. ) ;
#6339=SHAPE_REPRESENTATION_RELATIONSHIP ( 'NONE' , 'NONE' ,  #67568, #11074 ) ;
#6528=( LENGTH_UNIT ( ) NAMED_UNIT ( * ) SI_UNIT ( .MILLI., .METRE. ) );
#6679=( NAMED_UNIT ( * ) SI_UNIT ( $, .STERADIAN. ) SOLID_ANGLE_UNIT ( ) );
#6709=EDGE_CURVE ( 'NONE', #11138, #44728, #12790, .T. ) ;
#6733=( GEOMETRIC_REPRESENTATION_CONTEXT ( 3 ) GLOBAL_UNCERTAINTY_ASSIGNED_CONTEXT ( ( #12130 ) ) GLOBAL_UNIT_ASSIGNED_CONTEXT ( ( #39093, #44723, #33092 ) ) REPRESENTATION_CONTEXT ( 'NONE', 'WORKASPACE' ) );
#6920=CIRCLE ( 'NONE', #50722, 3.000000000000000444 ) ;
#7184=AXIS2_PLACEMENT_3D ( 'NONE', #39718, #49217, #40076 ) ;
#7217=DIRECTION ( 'NONE',  ( 0.000000000000000000, 0.000000000000000000, 1.000000000000000000 ) ) ;
#7258=SURFACE_STYLE_USAGE ( .BOTH. , #33631 ) ;
#7398=SURFACE_SIDE_STYLE ('',( #38414 ) ) ;
#8257=DIRECTION ( 'NONE',  ( -0.000000000000000000, -1.000000000000000000, -0.000000000000000000 ) ) ;
#8498=EDGE_CURVE ( 'NONE', #44728, #47926, #28711, .T. ) ;
#8505=DIRECTION ( 'NONE',  ( 0.000000000000000000, 0.000000000000000000, 1.000000000000000000 ) ) ;
#8897=DIRECTION ( 'NONE',  ( 0.000000000000000000, 0.000000000000000000, -1.000000000000000000 ) ) ;
#9683=AXIS2_PLACEMENT_3D ( 'NONE', #36066, #20566, #42083 ) ;
#10399=ORIENTED_EDGE ( 'NONE', *, *, #39600, .F. ) ;
#10931=UNCERTAINTY_MEASURE_WITH_UNIT (LENGTH_MEASURE( 1.000000000000000082E-05 ), #6528, 'distance_accuracy_value', 'NONE');
#11074=ADVANCED_BREP_SHAPE_REPRESENTATION ( '', ( #50379, #42840 ), #47260 ) ;
#11138=VERTEX_POINT ( 'NONE', #42296 ) ;
#11482=FILL_AREA_STYLE ('',( #50177 ) ) ;
#11710=AXIS2_PLACEMENT_3D ( 'NONE', #64111, #49024, #65144 ) ;
#12130=UNCERTAINTY_MEASURE_WITH_UNIT (LENGTH_MEASURE( 1.000000000000000082E-05 ), #39093, 'distance_accuracy_value', 'NONE');
#12173=CARTESIAN_POINT ( 'NONE',  ( 3.673940397442060361E-16, 2.299999999999999822, 3.000000000000000444 ) ) ;
#12633=AXIS2_PLACEMENT_3D ( 'NONE', #45860, #57076, #8897 ) ;
#12790=CIRCLE ( 'NONE', #7184, 10.00000000000000000 ) ;
#13011=FACE_OUTER_BOUND ( 'NONE', #24668, .T. ) ;
#13278=AXIS2_PLACEMENT_3D ( 'NONE', #58997, #48837, #26943 ) ;
#13763=CARTESIAN_POINT ( 'NONE',  ( 0.000000000000000000, 0.000000000000000000, 0.000000000000000000 ) ) ;
#13974=DIRECTION ( 'NONE',  ( 0.000000000000000000, 0.000000000000000000, 1.000000000000000000 ) ) ;
#14586=PLANE ( 'NONE',  #43268 ) ;
#15477=APPLICATION_CONTEXT ( 'automotive_design' ) ;
#15581=CARTESIAN_POINT ( 'NONE',  ( 0.000000000000000000, 0.000000000000000000, -10.00000000000000000 ) ) ;
#15592=VECTOR ( 'NONE', #39644, 1000.000000000000000 ) ;
#15597=FACE_OUTER_BOUND ( 'NONE', #33023, .T. ) ;
#15801=PRODUCT_DEFINITION_FORMATION_WITH_SPECIFIED_SOURCE ( 'ANY', '', #37873, .NOT_KNOWN. ) ;
#15933=ORIENTED_EDGE ( 'NONE', *, *, #52906, .F. ) ;
#16928=FILL_AREA_STYLE_COLOUR ( '', #35976 ) ;
#16950=DIRECTION ( 'NONE',  ( 0.000000000000000000, -0.000000000000000000, 1.000000000000000000 ) ) ;
#18167=CARTESIAN_POINT ( 'NONE',  ( 1.224646799147353256E-15, 0.000000000000000000, 10.00000000000000000 ) ) ;
#18354=CARTESIAN_POINT ( 'NONE',  ( 0.000000000000000000, 2.299999999999999822, 0.000000000000000000 ) ) ;
#18440=EDGE_CURVE ( 'NONE', #65168, #43714, #41770, .T. ) ;
#19079=CYLINDRICAL_SURFACE ( 'NONE', #12633, 10.00000000000000000 ) ;
#19135=PRODUCT_DEFINITION_CONTEXT ( 'detailed design', #15477, 'design' ) ;
#19227=CARTESIAN_POINT ( 'NONE',  ( 0.000000000000000000, 0.000000000000000000, 0.000000000000000000 ) ) ;
#20566=DIRECTION ( 'NONE',  ( 0.000000000000000000, 1.000000000000000000, 0.000000000000000000 ) ) ;
#20591=EDGE_CURVE ( 'NONE', #29559, #65168, #1866, .T. ) ;
#20869=CIRCLE ( 'NONE', #9683, 3.000000000000000444 ) ;
#21077=DIRECTION ( 'NONE',  ( -0.000000000000000000, -1.000000000000000000, -0.000000000000000000 ) ) ;
#21565=AXIS2_PLACEMENT_3D ( 'NONE', #2397, #45072, #56623 ) ;
#22208=PLANE ( 'NONE',  #64096 ) ;
#22516=MECHANICAL_DESIGN_GEOMETRIC_PRESENTATION_REPRESENTATION('',(#44980),#6733);
#22554=DIRECTION ( 'NONE',  ( 0.000000000000000000, 1.000000000000000000, 0.000000000000000000 ) ) ;
#22743=( NAMED_UNIT ( * ) PLANE_ANGLE_UNIT ( ) SI_UNIT ( $, .RADIAN. ) );
#23547=CARTESIAN_POINT ( 'NONE',  ( 1.224646799147353256E-15, 2.299999999999999822, 10.00000000000000000 ) ) ;
#23724=CARTESIAN_POINT ( 'NONE',  ( 0.000000000000000000, 2.299999999999999822, -3.000000000000000444 ) ) ;
#24188=AXIS2_PLACEMENT_3D ( 'NONE', #40956, #62694, #63420 ) ;
#24365=FACE_OUTER_BOUND ( 'NONE', #43002, .T. ) ;
#24668=EDGE_LOOP ( 'NONE', ( #10399, #69405, #44050, #15933 ) ) ;
#25799=ORIENTED_EDGE ( 'NONE', *, *, #49735, .T. ) ;
#26135=CLOSED_SHELL ( 'NONE', ( #57830, #54863, #45267, #38808, #27699, #60414 ) ) ;
#26326=EDGE_LOOP ( 'NONE', ( #51140, #39619 ) ) ;
#26943=DIRECTION ( 'NONE',  ( 0.000000000000000000, 0.000000000000000000, 1.000000000000000000 ) ) ;
#27116=PRODUCT_DEFINITION_SHAPE ( 'NONE', 'NONE',  #64860 ) ;
#27433=( LENGTH_UNIT ( ) NAMED_UNIT ( * ) SI_UNIT ( .MILLI., .METRE. ) );
#27691=COLOUR_RGB ( '', 0.66274510, 0.83137255, 0.94901961) ;
#27699=ADVANCED_FACE ( 'NONE', ( #15597 ), #3227, .T. ) ;
#28220=DIRECTION ( 'NONE',  ( 0.000000000000000000, 1.000000000000000000, 0.000000000000000000 ) ) ;
#28324=( NAMED_UNIT ( * ) SI_UNIT ( $, .STERADIAN. ) SOLID_ANGLE_UNIT ( ) );
#28470=( NAMED_UNIT ( * ) PLANE_ANGLE_UNIT ( ) SI_UNIT ( $, .RADIAN. ) );
#28711=LINE ( 'NONE', #66352, #45597 ) ;
#29074=ORIENTED_EDGE ( 'NONE', *, *, #39600, .T. ) ;
#29222=DIRECTION ( 'NONE',  ( 0.000000000000000000, 1.000000000000000000, 0.000000000000000000 ) ) ;
#29559=VERTEX_POINT ( 'NONE', #46822 ) ;
#30320=FACE_OUTER_BOUND ( 'NONE', #58349, .T. ) ;
#30382=FACE_OUTER_BOUND ( 'NONE', #54372, .T. ) ;
#30933=LINE ( 'NONE', #41885, #57991 ) ;
#32342=DIRECTION ( 'NONE',  ( 0.000000000000000000, 0.000000000000000000, 1.000000000000000000 ) ) ;
#33023=EDGE_LOOP ( 'NONE', ( #57498, #60719, #38947, #54205 ) ) ;
#33092=( NAMED_UNIT ( * ) SI_UNIT ( $, .STERADIAN. ) SOLID_ANGLE_UNIT ( ) );
#33118=FACE_OUTER_BOUND ( 'NONE', #37504, .T. ) ;
#33423=APPLICATION_CONTEXT ( 'automotive_design' ) ;
#33631=SURFACE_SIDE_STYLE ('',( #60695 ) ) ;
#35165=CYLINDRICAL_SURFACE ( 'NONE', #21565, 3.000000000000000444 ) ;
#35267=EDGE_CURVE ( 'NONE', #47926, #46046, #37294, .T. ) ;
#35627=STYLED_ITEM ( 'NONE', ( #60015 ), #50379 ) ;
#35976=COLOUR_RGB ( '', 0.66274510, 0.83137255, 0.94901961) ;
#36052=ORIENTED_EDGE ( 'NONE', *, *, #47226, .F. ) ;
#36066=CARTESIAN_POINT ( 'NONE',  ( 0.000000000000000000, 2.299999999999999822, 0.000000000000000000 ) ) ;
#36464=CIRCLE ( 'NONE', #11710, 10.00000000000000000 ) ;
#37071=ORIENTED_EDGE ( 'NONE', *, *, #18440, .F. ) ;
#37294=CIRCLE ( 'NONE', #2381, 10.00000000000000000 ) ;
#37504=EDGE_LOOP ( 'NONE', ( #61215, #5551 ) ) ;
#37768=CYLINDRICAL_SURFACE ( 'NONE', #55622, 3.000000000000000444 ) ;
#37873=PRODUCT ( '15. Washer M6', '15. Washer M6', '', ( #55041 ) ) ;
#38201=ORIENTED_EDGE ( 'NONE', *, *, #8498, .T. ) ;
#38414=SURFACE_STYLE_FILL_AREA ( #44033 ) ;
#38808=ADVANCED_FACE ( 'NONE', ( #30382, #41348 ), #14586, .F. ) ;
#38947=ORIENTED_EDGE ( 'NONE', *, *, #4351, .T. ) ;
#39093=( LENGTH_UNIT ( ) NAMED_UNIT ( * ) SI_UNIT ( .MILLI., .METRE. ) );
#39600=EDGE_CURVE ( 'NONE', #2089, #43714, #30933, .T. ) ;
#39619=ORIENTED_EDGE ( 'NONE', *, *, #52906, .T. ) ;
#39644=DIRECTION ( 'NONE',  ( -0.000000000000000000, -1.000000000000000000, -0.000000000000000000 ) ) ;
#39718=CARTESIAN_POINT ( 'NONE',  ( 0.000000000000000000, 2.299999999999999822, 0.000000000000000000 ) ) ;
#40076=DIRECTION ( 'NONE',  ( 0.000000000000000000, 0.000000000000000000, 1.000000000000000000 ) ) ;
#40736=DIRECTION ( 'NONE',  ( 0.000000000000000000, 1.000000000000000000, 0.000000000000000000 ) ) ;
#40956=CARTESIAN_POINT ( 'NONE',  ( 0.000000000000000000, 2.299999999999999822, 0.000000000000000000 ) ) ;
#41348=FACE_BOUND ( 'NONE', #26326, .T. ) ;
#41770=CIRCLE ( 'NONE', #1242, 3.000000000000000444 ) ;
#41885=CARTESIAN_POINT ( 'NONE',  ( 3.673940397442060361E-16, 2.299999999999999822, 3.000000000000000444 ) ) ;
#42016=ORIENTED_EDGE ( 'NONE', *, *, #20591, .F. ) ;
#42083=DIRECTION ( 'NONE',  ( 0.000000000000000000, 0.000000000000000000, 1.000000000000000000 ) ) ;
#42296=CARTESIAN_POINT ( 'NONE',  ( 0.000000000000000000, 2.299999999999999822, -10.00000000000000000 ) ) ;
#42397=MECHANICAL_DESIGN_GEOMETRIC_PRESENTATION_REPRESENTATION('',(#35627),#48020);
#42840=AXIS2_PLACEMENT_3D ( 'NONE', #59977, #7217, #49786 ) ;
#43002=EDGE_LOOP ( 'NONE', ( #9, #38201, #66515, #51838 ) ) ;
#43268=AXIS2_PLACEMENT_3D ( 'NONE', #43462, #48719, #5387 ) ;
#43399=DIRECTION ( 'NONE',  ( 0.000000000000000000, 0.000000000000000000, -1.000000000000000000 ) ) ;
#43462=CARTESIAN_POINT ( 'NONE',  ( 0.000000000000000000, 0.000000000000000000, 0.000000000000000000 ) ) ;
#43714=VERTEX_POINT ( 'NONE', #4138 ) ;
#44033=FILL_AREA_STYLE ('',( #16928 ) ) ;
#44050=ORIENTED_EDGE ( 'NONE', *, *, #20591, .T. ) ;
#44556=UNCERTAINTY_MEASURE_WITH_UNIT (LENGTH_MEASURE( 1.000000000000000082E-05 ), #27433, 'distance_accuracy_value', 'NONE');
#44598=CARTESIAN_POINT ( 'NONE',  ( 0.000000000000000000, 2.299999999999999822, -10.00000000000000000 ) ) ;
#44723=( NAMED_UNIT ( * ) PLANE_ANGLE_UNIT ( ) SI_UNIT ( $, .RADIAN. ) );
#44728=VERTEX_POINT ( 'NONE', #23547 ) ;
#44980=STYLED_ITEM ( 'NONE', ( #49978 ), #11074 ) ;
#45072=DIRECTION ( 'NONE',  ( -0.000000000000000000, -1.000000000000000000, -0.000000000000000000 ) ) ;
#45267=ADVANCED_FACE ( 'NONE', ( #33118, #65096 ), #22208, .T. ) ;
#45597=VECTOR ( 'NONE', #55096, 1000.000000000000000 ) ;
#45860=CARTESIAN_POINT ( 'NONE',  ( 0.000000000000000000, 2.299999999999999822, 0.000000000000000000 ) ) ;
#46046=VERTEX_POINT ( 'NONE', #15581 ) ;
#46822=CARTESIAN_POINT ( 'NONE',  ( 0.000000000000000000, 2.299999999999999822, -3.000000000000000444 ) ) ;
#47226=EDGE_CURVE ( 'NONE', #2089, #29559, #52128, .T. ) ;
#47260=( GEOMETRIC_REPRESENTATION_CONTEXT ( 3 ) GLOBAL_UNCERTAINTY_ASSIGNED_CONTEXT ( ( #44556 ) ) GLOBAL_UNIT_ASSIGNED_CONTEXT ( ( #27433, #28470, #6679 ) ) REPRESENTATION_CONTEXT ( 'NONE', 'WORKASPACE' ) );
#47527=AXIS2_PLACEMENT_3D ( 'NONE', #18354, #29222, #32342 ) ;
#47926=VERTEX_POINT ( 'NONE', #18167 ) ;
#48020=( GEOMETRIC_REPRESENTATION_CONTEXT ( 3 ) GLOBAL_UNCERTAINTY_ASSIGNED_CONTEXT ( ( #10931 ) ) GLOBAL_UNIT_ASSIGNED_CONTEXT ( ( #6528, #22743, #28324 ) ) REPRESENTATION_CONTEXT ( 'NONE', 'WORKASPACE' ) );
#48719=DIRECTION ( 'NONE',  ( 0.000000000000000000, 1.000000000000000000, 0.000000000000000000 ) ) ;
#48833=ORIENTED_EDGE ( 'NONE', *, *, #63046, .F. ) ;
#48837=DIRECTION ( 'NONE',  ( 0.000000000000000000, 1.000000000000000000, 0.000000000000000000 ) ) ;
#49002=DIRECTION ( 'NONE',  ( -0.000000000000000000, -1.000000000000000000, -0.000000000000000000 ) ) ;
#49024=DIRECTION ( 'NONE',  ( 0.000000000000000000, 1.000000000000000000, 0.000000000000000000 ) ) ;
#49217=DIRECTION ( 'NONE',  ( 0.000000000000000000, 1.000000000000000000, 0.000000000000000000 ) ) ;
#49735=EDGE_CURVE ( 'NONE', #29559, #2089, #20869, .T. ) ;
#49786=DIRECTION ( 'NONE',  ( 1.000000000000000000, 0.000000000000000000, 0.000000000000000000 ) ) ;
#49793=SHAPE_DEFINITION_REPRESENTATION ( #27116, #67568 ) ;
#49978=PRESENTATION_STYLE_ASSIGNMENT (( #59813 ) ) ;
#50177=FILL_AREA_STYLE_COLOUR ( '', #27691 ) ;
#50379=MANIFOLD_SOLID_BREP ( 'Boss-Extrude1', #26135 ) ;
#50722=AXIS2_PLACEMENT_3D ( 'NONE', #19227, #40736, #13974 ) ;
#51140=ORIENTED_EDGE ( 'NONE', *, *, #18440, .T. ) ;
#51838=ORIENTED_EDGE ( 'NONE', *, *, #4351, .F. ) ;
#52128=CIRCLE ( 'NONE', #47527, 3.000000000000000444 ) ;
#52906=EDGE_CURVE ( 'NONE', #43714, #65168, #6920, .T. ) ;
#54205=ORIENTED_EDGE ( 'NONE', *, *, #63046, .T. ) ;
#54372=EDGE_LOOP ( 'NONE', ( #48833, #66306 ) ) ;
#54863=ADVANCED_FACE ( 'NONE', ( #24365 ), #19079, .T. ) ;
#55041=PRODUCT_CONTEXT ( 'NONE', #33423, 'mechanical' ) ;
#55096=DIRECTION ( 'NONE',  ( -0.000000000000000000, -1.000000000000000000, -0.000000000000000000 ) ) ;
#55240=CARTESIAN_POINT ( 'NONE',  ( 0.000000000000000000, 2.299999999999999822, 0.000000000000000000 ) ) ;
#55622=AXIS2_PLACEMENT_3D ( 'NONE', #1026, #49002, #43399 ) ;
#56623=DIRECTION ( 'NONE',  ( 0.000000000000000000, 0.000000000000000000, -1.000000000000000000 ) ) ;
#56679=DIRECTION ( 'NONE',  ( 0.000000000000000000, 1.000000000000000000, 0.000000000000000000 ) ) ;
#57076=DIRECTION ( 'NONE',  ( -0.000000000000000000, -1.000000000000000000, -0.000000000000000000 ) ) ;
#57215=VECTOR ( 'NONE', #8257, 1000.000000000000000 ) ;
#57498=ORIENTED_EDGE ( 'NONE', *, *, #8498, .F. ) ;
#57830=ADVANCED_FACE ( 'NONE', ( #30320 ), #37768, .F. ) ;
#57991=VECTOR ( 'NONE', #21077, 1000.000000000000000 ) ;
#58349=EDGE_LOOP ( 'NONE', ( #25799, #29074, #37071, #42016 ) ) ;
#58997=CARTESIAN_POINT ( 'NONE',  ( 0.000000000000000000, 2.299999999999999822, 0.000000000000000000 ) ) ;
#59813=SURFACE_STYLE_USAGE ( .BOTH. , #7398 ) ;
#59977=CARTESIAN_POINT ( 'NONE',  ( 0.000000000000000000, 0.000000000000000000, 0.000000000000000000 ) ) ;
#60015=PRESENTATION_STYLE_ASSIGNMENT (( #7258 ) ) ;
#60414=ADVANCED_FACE ( 'NONE', ( #13011 ), #35165, .F. ) ;
#60695=SURFACE_STYLE_FILL_AREA ( #11482 ) ;
#60719=ORIENTED_EDGE ( 'NONE', *, *, #6709, .F. ) ;
#61215=ORIENTED_EDGE ( 'NONE', *, *, #6709, .T. ) ;
#61536=EDGE_LOOP ( 'NONE', ( #3994, #36052 ) ) ;
#62694=DIRECTION ( 'NONE',  ( -0.000000000000000000, -1.000000000000000000, -0.000000000000000000 ) ) ;
#62742=CIRCLE ( 'NONE', #13278, 10.00000000000000000 ) ;
#63046=EDGE_CURVE ( 'NONE', #46046, #47926, #36464, .T. ) ;
#63420=DIRECTION ( 'NONE',  ( 0.000000000000000000, 0.000000000000000000, -1.000000000000000000 ) ) ;
#64096=AXIS2_PLACEMENT_3D ( 'NONE', #55240, #22554, #16950 ) ;
#64111=CARTESIAN_POINT ( 'NONE',  ( 0.000000000000000000, 0.000000000000000000, 0.000000000000000000 ) ) ;
#64860=PRODUCT_DEFINITION ( 'UNKNOWN', '', #15801, #19135 ) ;
#65096=FACE_BOUND ( 'NONE', #61536, .T. ) ;
#65144=DIRECTION ( 'NONE',  ( 0.000000000000000000, 0.000000000000000000, 1.000000000000000000 ) ) ;
#65168=VERTEX_POINT ( 'NONE', #5099 ) ;
#65655=LINE ( 'NONE', #44598, #15592 ) ;
#66229=CARTESIAN_POINT ( 'NONE',  ( 0.000000000000000000, 0.000000000000000000, 0.000000000000000000 ) ) ;
#66306=ORIENTED_EDGE ( 'NONE', *, *, #35267, .F. ) ;
#66352=CARTESIAN_POINT ( 'NONE',  ( 1.224646799147353256E-15, 2.299999999999999822, 10.00000000000000000 ) ) ;
#66515=ORIENTED_EDGE ( 'NONE', *, *, #35267, .T. ) ;
#67568=SHAPE_REPRESENTATION ( '15. Washer M6', ( #42840 ), #47260 ) ;
#69405=ORIENTED_EDGE ( 'NONE', *, *, #47226, .T. ) ;
ENDSEC;
END-ISO-10303-21;
